ISO-10303-21;
HEADER;
FILE_DESCRIPTION (('STEP AP214'),
    '1' );
FILE_NAME ('socket head cap screw_iso_ISO 4762 M5 x 25 - 25N.step',
    '2026-10-08T12:12:07',
    ( '' ),
    ( '' ),
    'SwSTEP 2.0',
    'SolidWorks 2026',
    '' );
FILE_SCHEMA (( 'AUTOMOTIVE_DESIGN' ));
ENDSEC;

DATA;
#21=( LENGTH_UNIT ( ) NAMED_UNIT ( * ) SI_UNIT ( .MILLI., .METRE. ) );
#40=PLANE ( 'NONE',  #657 ) ;
#47=ORIENTED_EDGE ( 'NONE', *, *, #2802, .T. ) ;
#68=FACE_OUTER_BOUND ( 'NONE', #3488, .T. ) ;
#75=ORIENTED_EDGE ( 'NONE', *, *, #2802, .F. ) ;
#78=DIRECTION ( 'NONE',  ( -1.000000000000000000, 0.000000000000000000, 0.000000000000000000 ) ) ;
#79=DIRECTION ( 'NONE',  ( 0.000000000000000000, -0.5000000000000009992, -0.8660254037844380415 ) ) ;
#86=ORIENTED_EDGE ( 'NONE', *, *, #5141, .F. ) ;
#105=ADVANCED_FACE ( 'NONE', ( #1577 ), #6609, .T. ) ;
#117=VERTEX_POINT ( 'NONE', #5975 ) ;
#182=ORIENTED_EDGE ( 'NONE', *, *, #753, .T. ) ;
#185=CARTESIAN_POINT ( 'NONE',  ( 2.500000000000002220, -1.178949249685215417, 2.042000000000002036 ) ) ;
#190=CARTESIAN_POINT ( 'NONE',  ( 2.500000000000002220, 1.178949249685212086, -2.042000000000002036 ) ) ;
#200=ORIENTED_EDGE ( 'NONE', *, *, #5028, .F. ) ;
#204=FACE_OUTER_BOUND ( 'NONE', #353, .T. ) ;
#205=AXIS2_PLACEMENT_3D ( 'NONE', #4806, #5391, #4058 ) ;
#211=CARTESIAN_POINT ( 'NONE',  ( 2.500000000000002220, -1.178949249685215417, 2.042000000000002036 ) ) ;
#222=EDGE_CURVE ( 'NONE', #3673, #8139, #7510, .T. ) ;
#225=ORIENTED_EDGE ( 'NONE', *, *, #1635, .F. ) ;
#241=EDGE_CURVE ( 'NONE', #2831, #8109, #2243, .T. ) ;
#244=VERTEX_POINT ( 'NONE', #4816 ) ;
#250=LINE ( 'NONE', #1476, #2497 ) ;
#257=DIRECTION ( 'NONE',  ( 0.000000000000000000, 0.8660254037844380415, -0.5000000000000009992 ) ) ;
#259=EDGE_CURVE ( 'NONE', #2258, #2818, #4701, .T. ) ;
#295=CARTESIAN_POINT ( 'NONE',  ( 2.500000000000002220, 1.768423874527826678, 1.020999999999997687 ) ) ;
#297=DIRECTION ( 'NONE',  ( 0.000000000000000000, 0.5000000000000009992, 0.8660254037844380415 ) ) ;
#304=DIRECTION ( 'NONE',  ( 1.000000000000000000, 0.000000000000000000, 0.000000000000000000 ) ) ;
#317=LINE ( 'NONE', #2196, #5299 ) ;
#344=PLANE ( 'NONE',  #4474 ) ;
#345=CYLINDRICAL_SURFACE ( 'NONE', #7671, 2.500000000000000444 ) ;
#353=EDGE_LOOP ( 'NONE', ( #7067, #4425, #6961, #3331 ) ) ;
#356=DIRECTION ( 'NONE',  ( 0.000000000000000000, -1.000000000000000000, 0.000000000000000000 ) ) ;
#359=AXIS2_PLACEMENT_3D ( 'NONE', #4680, #2767, #7953 ) ;
#380=LINE ( 'NONE', #2927, #3726 ) ;
#408=DIRECTION ( 'NONE',  ( 0.000000000000000000, 0.8660254037844391517, 0.4999999999999991673 ) ) ;
#441=EDGE_LOOP ( 'NONE', ( #6776, #4989, #6704, #8166, #5130 ) ) ;
#450=AXIS2_PLACEMENT_3D ( 'NONE', #1025, #3572, #7430 ) ;
#456=CARTESIAN_POINT ( 'NONE',  ( 30.00000000000000000, 0.000000000000000000, 2.054999999999993054 ) ) ;
#459=UNCERTAINTY_MEASURE_WITH_UNIT (LENGTH_MEASURE( 1.000000000000000082E-05 ), #722, 'distance_accuracy_value', 'NONE');
#494=CARTESIAN_POINT ( 'NONE',  ( 0.000000000000000000, -1.178949249685215417, 2.042000000000002036 ) ) ;
#499=SHAPE_REPRESENTATION ( 'socket head cap screw_iso_ISO 4762 M5 x 25 - 25N', ( #1587 ), #6006 ) ;
#504=ADVANCED_FACE ( 'NONE', ( #5237, #6000 ), #4603, .T. ) ;
#516=CONICAL_SURFACE ( 'NONE', #4902, 2.041999999999999815, 1.047197551196591858 ) ;
#524=CARTESIAN_POINT ( 'NONE',  ( 2.500000000000002220, 3.469446951953614189E-15, 2.041999999999998483 ) ) ;
#528=CARTESIAN_POINT ( 'NONE',  ( 2.500000000000015987, 1.768423874527823347, -1.021000000000001018 ) ) ;
#551=EDGE_CURVE ( 'NONE', #4688, #1969, #7750, .T. ) ;
#553=EDGE_LOOP ( 'NONE', ( #5009, #47, #1841 ) ) ;
#567=CARTESIAN_POINT ( 'NONE',  ( 2.500000000000002220, 2.357898499370434386, -3.469446951953614189E-15 ) ) ;
#592=ORIENTED_EDGE ( 'NONE', *, *, #7163, .F. ) ;
#608=DIRECTION ( 'NONE',  ( -1.000000000000000000, 0.000000000000000000, 0.000000000000000000 ) ) ;
#649=CARTESIAN_POINT ( 'NONE',  ( 30.00000000000000000, 0.000000000000000000, 2.054999999999993054 ) ) ;
#653=AXIS2_PLACEMENT_3D ( 'NONE', #5260, #6029, #840 ) ;
#655=FACE_OUTER_BOUND ( 'NONE', #553, .T. ) ;
#657=AXIS2_PLACEMENT_3D ( 'NONE', #2591, #1967, #4493 ) ;
#662=CARTESIAN_POINT ( 'NONE',  ( 0.000000000000000000, 2.357898499370434386, -3.469446951953614189E-15 ) ) ;
#663=CARTESIAN_POINT ( 'NONE',  ( 2.500000000000002220, -1.768423874527823347, 1.021000000000001018 ) ) ;
#670=AXIS2_PLACEMENT_3D ( 'NONE', #1126, #3587, #2375 ) ;
#681=ORIENTED_EDGE ( 'NONE', *, *, #259, .T. ) ;
#705=EDGE_LOOP ( 'NONE', ( #7620, #3737, #5363, #7417 ) ) ;
#709=EDGE_LOOP ( 'NONE', ( #7570, #5169, #7796, #3889 ) ) ;
#722=( LENGTH_UNIT ( ) NAMED_UNIT ( * ) SI_UNIT ( .MILLI., .METRE. ) );
#733=LINE ( 'NONE', #185, #5672 ) ;
#738=ADVANCED_FACE ( 'NONE', ( #7614 ), #40, .T. ) ;
#742=VECTOR ( 'NONE', #4927, 1000.000000000000000 ) ;
#753=EDGE_CURVE ( 'NONE', #3217, #4939, #8128, .T. ) ;
#822=ORIENTED_EDGE ( 'NONE', *, *, #6373, .T. ) ;
#840=DIRECTION ( 'NONE',  ( 0.000000000000000000, 0.000000000000000000, -1.000000000000000000 ) ) ;
#869=VECTOR ( 'NONE', #4101, 1000.000000000000000 ) ;
#887=DIRECTION ( 'NONE',  ( 0.000000000000000000, 0.000000000000000000, -1.000000000000000000 ) ) ;
#889=DIRECTION ( 'NONE',  ( 0.000000000000000000, 1.000000000000000000, 1.224646799147353207E-16 ) ) ;
#901=AXIS2_PLACEMENT_3D ( 'NONE', #4113, #6637, #1534 ) ;
#917=DIRECTION ( 'NONE',  ( -1.000000000000000000, 0.000000000000000000, 0.000000000000000000 ) ) ;
#921=AXIS2_PLACEMENT_3D ( 'NONE', #2556, #5098, #7618 ) ;
#924=DIRECTION ( 'NONE',  ( -1.000000000000000000, 0.000000000000000000, 0.000000000000000000 ) ) ;
#928=AXIS2_PLACEMENT_3D ( 'NONE', #6347, #6456, #5688 ) ;
#932=CARTESIAN_POINT ( 'NONE',  ( 5.000000000000015099, 4.250000000000000000, 0.000000000000000000 ) ) ;
#933=CARTESIAN_POINT ( 'NONE',  ( 3.678949249685231848, 0.000000000000000000, -6.938893903907228378E-15 ) ) ;
#965=( GEOMETRIC_REPRESENTATION_CONTEXT ( 3 ) GLOBAL_UNCERTAINTY_ASSIGNED_CONTEXT ( ( #7136 ) ) GLOBAL_UNIT_ASSIGNED_CONTEXT ( ( #21, #2607, #1985 ) ) REPRESENTATION_CONTEXT ( 'NONE', 'WORKASPACE' ) );
#971=ADVANCED_FACE ( 'NONE', ( #6529 ), #2576, .T. ) ;
#989=DIRECTION ( 'NONE',  ( -1.000000000000000000, 0.000000000000000000, 0.000000000000000000 ) ) ;
#992=VERTEX_POINT ( 'NONE', #3203 ) ;
#1010=CARTESIAN_POINT ( 'NONE',  ( 2.500000000000002220, 2.357898499370434386, -3.469446951953614189E-15 ) ) ;
#1025=CARTESIAN_POINT ( 'NONE',  ( 5.200000000000020606, 0.000000000000000000, -6.938893903907228378E-15 ) ) ;
#1029=FACE_OUTER_BOUND ( 'NONE', #1141, .T. ) ;
#1034=ADVANCED_FACE ( 'NONE', ( #655 ), #5850, .F. ) ;
#1037=VERTEX_POINT ( 'NONE', #3239 ) ;
#1049=VECTOR ( 'NONE', #4012, 1000.000000000000000 ) ;
#1058=EDGE_CURVE ( 'NONE', #6819, #2818, #1552, .T. ) ;
#1087=ORIENTED_EDGE ( 'NONE', *, *, #5273, .F. ) ;
#1088=DIRECTION ( 'NONE',  ( -1.000000000000000000, 0.000000000000000000, 0.000000000000000000 ) ) ;
#1089=ORIENTED_EDGE ( 'NONE', *, *, #551, .T. ) ;
#1110=VERTEX_POINT ( 'NONE', #1606 ) ;
#1126=CARTESIAN_POINT ( 'NONE',  ( 0.2500000000000002220, 0.000000000000000000, 2.081668171172168513E-14 ) ) ;
#1139=CARTESIAN_POINT ( 'NONE',  ( 2.500000000000002220, 2.357898499370434386, -3.469446951953614189E-15 ) ) ;
#1141=EDGE_LOOP ( 'NONE', ( #7138, #4109, #4365, #6940, #3679 ) ) ;
#1157=VECTOR ( 'NONE', #917, 1000.000000000000000 ) ;
#1163=ADVANCED_FACE ( 'NONE', ( #2760 ), #2066, .T. ) ;
#1182=VECTOR ( 'NONE', #8132, 1000.000000000000000 ) ;
#1185=PLANE ( 'NONE',  #6273 ) ;
#1203=ORIENTED_EDGE ( 'NONE', *, *, #2986, .F. ) ;
#1207=DIRECTION ( 'NONE',  ( 0.000000000000000000, 0.000000000000000000, 1.000000000000000000 ) ) ;
#1208=CARTESIAN_POINT ( 'NONE',  ( 2.500000000000002220, 2.357898499370434386, -3.469446951953614189E-15 ) ) ;
#1212=EDGE_CURVE ( 'NONE', #6705, #244, #6254, .T. ) ;
#1213=EDGE_LOOP ( 'NONE', ( #6439, #7962 ) ) ;
#1228=AXIS2_PLACEMENT_3D ( 'NONE', #4153, #3575, #6588 ) ;
#1235=VERTEX_POINT ( 'NONE', #5473 ) ;
#1236=ADVANCED_FACE ( 'NONE', ( #2392 ), #3003, .F. ) ;
#1266=ORIENTED_EDGE ( 'NONE', *, *, #1957, .F. ) ;
#1288=LINE ( 'NONE', #662, #7146 ) ;
#1295=EDGE_LOOP ( 'NONE', ( #7925, #7105 ) ) ;
#1353=VECTOR ( 'NONE', #6533, 1000.000000000000000 ) ;
#1360=( NAMED_UNIT ( * ) PLANE_ANGLE_UNIT ( ) SI_UNIT ( $, .RADIAN. ) );
#1383=MECHANICAL_DESIGN_GEOMETRIC_PRESENTATION_REPRESENTATION('',(#7478),#965);
#1410=DIRECTION ( 'NONE',  ( 0.000000000000000000, 0.000000000000000000, -1.000000000000000000 ) ) ;
#1414=CARTESIAN_POINT ( 'NONE',  ( 5.000000000000015099, 0.000000000000000000, 0.000000000000000000 ) ) ;
#1434=PRESENTATION_STYLE_ASSIGNMENT (( #5798 ) ) ;
#1437=STYLED_ITEM ( 'NONE', ( #3738 ), #6901 ) ;
#1441=CIRCLE ( 'NONE', #7669, 4.250000000000000000 ) ;
#1446=AXIS2_PLACEMENT_3D ( 'NONE', #1208, #5779, #4320 ) ;
#1463=LINE ( 'NONE', #2826, #5036 ) ;
#1474=LINE ( 'NONE', #3414, #1049 ) ;
#1476=CARTESIAN_POINT ( 'NONE',  ( 0.000000000000000000, 2.357898499370434386, -3.469446951953614189E-15 ) ) ;
#1492=VECTOR ( 'NONE', #1529, 1000.000000000000114 ) ;
#1493=CARTESIAN_POINT ( 'NONE',  ( 2.500000000000002220, 2.357898499370434386, -3.469446951953614189E-15 ) ) ;
#1523=CARTESIAN_POINT ( 'NONE',  ( 5.200000000000020606, 0.000000000000000000, -6.938893903907228378E-15 ) ) ;
#1525=LINE ( 'NONE', #4028, #869 ) ;
#1529=DIRECTION ( 'NONE',  ( 0.000000000000000000, -0.5000000000000011102, -0.8660254037844379305 ) ) ;
#1534=DIRECTION ( 'NONE',  ( 0.000000000000000000, 0.000000000000000000, 1.000000000000000000 ) ) ;
#1541=EDGE_CURVE ( 'NONE', #3673, #5642, #1677, .T. ) ;
#1546=DIRECTION ( 'NONE',  ( 0.000000000000000000, 0.000000000000000000, 1.000000000000000000 ) ) ;
#1549=DIRECTION ( 'NONE',  ( -1.000000000000000000, -0.000000000000000000, -0.000000000000000000 ) ) ;
#1552=LINE ( 'NONE', #7780, #1353 ) ;
#1558=ORIENTED_EDGE ( 'NONE', *, *, #6373, .F. ) ;
#1570=FACE_OUTER_BOUND ( 'NONE', #6194, .T. ) ;
#1571=ORIENTED_EDGE ( 'NONE', *, *, #8156, .F. ) ;
#1577=FACE_OUTER_BOUND ( 'NONE', #5280, .T. ) ;
#1582=EDGE_CURVE ( 'NONE', #8109, #1110, #5914, .T. ) ;
#1587=AXIS2_PLACEMENT_3D ( 'NONE', #3942, #5152, #6454 ) ;
#1606=CARTESIAN_POINT ( 'NONE',  ( 0.000000000000000000, 5.051668046482844583E-16, -4.000000000000000000 ) ) ;
#1616=DIRECTION ( 'NONE',  ( -1.000000000000000000, 0.000000000000000000, 0.000000000000000000 ) ) ;
#1632=EDGE_LOOP ( 'NONE', ( #3081, #3214, #592, #225, #4957 ) ) ;
#1633=ORIENTED_EDGE ( 'NONE', *, *, #6648, .T. ) ;
#1635=EDGE_CURVE ( 'NONE', #992, #244, #7584, .T. ) ;
#1655=EDGE_CURVE ( 'NONE', #7104, #7111, #5666, .T. ) ;
#1677=LINE ( 'NONE', #6195, #742 ) ;
#1698=ORIENTED_EDGE ( 'NONE', *, *, #1058, .T. ) ;
#1724=ORIENTED_EDGE ( 'NONE', *, *, #2446, .T. ) ;
#1725=CARTESIAN_POINT ( 'NONE',  ( 0.000000000000000000, 0.000000000000000000, 0.000000000000000000 ) ) ;
#1728=ORIENTED_EDGE ( 'NONE', *, *, #3275, .T. ) ;
#1755=CARTESIAN_POINT ( 'NONE',  ( 0.2500000000000002220, 0.000000000000000000, 2.081668171172168513E-14 ) ) ;
#1779=PLANE ( 'NONE',  #5951 ) ;
#1803=DIRECTION ( 'NONE',  ( 0.000000000000000000, -0.5000000000000009992, -0.8660254037844380415 ) ) ;
#1808=ORIENTED_EDGE ( 'NONE', *, *, #3629, .T. ) ;
#1819=ORIENTED_EDGE ( 'NONE', *, *, #2756, .T. ) ;
#1833=DIRECTION ( 'NONE',  ( 0.000000000000000000, -0.4999999999999991118, 0.8660254037844390407 ) ) ;
#1841=ORIENTED_EDGE ( 'NONE', *, *, #5379, .F. ) ;
#1856=AXIS2_PLACEMENT_3D ( 'NONE', #7030, #1936, #3040 ) ;
#1882=CARTESIAN_POINT ( 'NONE',  ( 2.500000000000002220, 0.000000000000000000, 0.000000000000000000 ) ) ;
#1902=ORIENTED_EDGE ( 'NONE', *, *, #2805, .T. ) ;
#1936=DIRECTION ( 'NONE',  ( -1.000000000000000000, 0.000000000000000000, 0.000000000000000000 ) ) ;
#1951=DIRECTION ( 'NONE',  ( 0.000000000000000000, -0.4999999999999992228, 0.8660254037844390407 ) ) ;
#1954=CARTESIAN_POINT ( 'NONE',  ( -31.74999999999994316, 0.000000000000000000, 0.000000000000000000 ) ) ;
#1957=EDGE_CURVE ( 'NONE', #4688, #117, #6136, .T. ) ;
#1961=CARTESIAN_POINT ( 'NONE',  ( 2.500000000000002220, -1.178949249685215417, 2.042000000000002036 ) ) ;
#1967=DIRECTION ( 'NONE',  ( 1.000000000000000000, 0.000000000000000000, 0.000000000000000000 ) ) ;
#1969=VERTEX_POINT ( 'NONE', #528 ) ;
#1976=( GEOMETRIC_REPRESENTATION_CONTEXT ( 3 ) GLOBAL_UNCERTAINTY_ASSIGNED_CONTEXT ( ( #4873 ) ) GLOBAL_UNIT_ASSIGNED_CONTEXT ( ( #3604, #3010, #4941 ) ) REPRESENTATION_CONTEXT ( 'NONE', 'WORKASPACE' ) );
#1977=ORIENTED_EDGE ( 'NONE', *, *, #3275, .F. ) ;
#1985=( NAMED_UNIT ( * ) SI_UNIT ( $, .STERADIAN. ) SOLID_ANGLE_UNIT ( ) );
#2007=CARTESIAN_POINT ( 'NONE',  ( 5.200000000000020606, 0.000000000000000000, -6.938893903907228378E-15 ) ) ;
#2020=AXIS2_PLACEMENT_3D ( 'NONE', #1954, #608, #4482 ) ;
#2040=DIRECTION ( 'NONE',  ( -1.000000000000000000, 0.000000000000000000, 0.000000000000000000 ) ) ;
#2065=DIRECTION ( 'NONE',  ( 0.000000000000000000, 0.000000000000000000, 1.000000000000000000 ) ) ;
#2066=PLANE ( 'NONE',  #5073 ) ;
#2072=FACE_BOUND ( 'NONE', #6257, .T. ) ;
#2109=DIRECTION ( 'NONE',  ( 0.000000000000000000, 1.000000000000000000, -1.103561164596346103E-15 ) ) ;
#2139=DIRECTION ( 'NONE',  ( -1.000000000000000000, 0.000000000000000000, 0.000000000000000000 ) ) ;
#2145=DIRECTION ( 'NONE',  ( 0.000000000000000000, 0.000000000000000000, -1.000000000000000000 ) ) ;
#2196=CARTESIAN_POINT ( 'NONE',  ( 2.500000000000002220, -1.178949249685215417, 2.042000000000002036 ) ) ;
#2203=ORIENTED_EDGE ( 'NONE', *, *, #6591, .F. ) ;
#2230=ADVANCED_FACE ( 'NONE', ( #5552 ), #1185, .F. ) ;
#2241=AXIS2_PLACEMENT_3D ( 'NONE', #4060, #889, #3559 ) ;
#2243=CIRCLE ( 'NONE', #6885, 0.2500000000000002220 ) ;
#2252=VECTOR ( 'NONE', #3038, 1000.000000000000000 ) ;
#2258=VERTEX_POINT ( 'NONE', #6922 ) ;
#2263=FACE_OUTER_BOUND ( 'NONE', #441, .T. ) ;
#2282=DIRECTION ( 'NONE',  ( 0.000000000000000000, 0.000000000000000000, -1.000000000000000000 ) ) ;
#2309=CARTESIAN_POINT ( 'NONE',  ( 29.55500000000002458, 0.000000000000000000, 2.499999999999987121 ) ) ;
#2326=CARTESIAN_POINT ( 'NONE',  ( 30.00000000000000000, 2.789133085058097101E-16, -2.055000000000006821 ) ) ;
#2338=CARTESIAN_POINT ( 'NONE',  ( 2.500000000000002220, 0.000000000000000000, 0.000000000000000000 ) ) ;
#2342=DIRECTION ( 'NONE',  ( -0.5000000000000051070, 1.060575238724903217E-16, -0.8660254037844355990 ) ) ;
#2372=ORIENTED_EDGE ( 'NONE', *, *, #6735, .F. ) ;
#2375=DIRECTION ( 'NONE',  ( 0.000000000000000000, 0.000000000000000000, 1.000000000000000000 ) ) ;
#2392=FACE_OUTER_BOUND ( 'NONE', #6196, .T. ) ;
#2406=ADVANCED_FACE ( 'NONE', ( #1570 ), #3521, .T. ) ;
#2414=DIRECTION ( 'NONE',  ( 1.000000000000000000, -0.000000000000000000, -0.000000000000000000 ) ) ;
#2431=DIRECTION ( 'NONE',  ( 0.000000000000000000, 0.000000000000000000, 1.000000000000000000 ) ) ;
#2446=EDGE_CURVE ( 'NONE', #6378, #4032, #5359, .T. ) ;
#2454=CARTESIAN_POINT ( 'NONE',  ( 0.000000000000000000, 2.357898499370434386, -3.469446951953614189E-15 ) ) ;
#2463=FACE_OUTER_BOUND ( 'NONE', #705, .T. ) ;
#2492=EDGE_CURVE ( 'NONE', #6378, #1969, #7214, .T. ) ;
#2497=VECTOR ( 'NONE', #5226, 1000.000000000000114 ) ;
#2516=LINE ( 'NONE', #3266, #7031 ) ;
#2526=ORIENTED_EDGE ( 'NONE', *, *, #3007, .T. ) ;
#2544=CARTESIAN_POINT ( 'NONE',  ( 5.200000000000020606, 0.000000000000000000, -6.938893903907228378E-15 ) ) ;
#2556=CARTESIAN_POINT ( 'NONE',  ( 5.200000000000020606, 0.000000000000000000, -2.700000000000007727 ) ) ;
#2564=CARTESIAN_POINT ( 'NONE',  ( 2.500000000000002220, -1.178949249685218970, -2.041999999999998483 ) ) ;
#2568=FILL_AREA_STYLE_COLOUR ( '', #4158 ) ;
#2570=ADVANCED_FACE ( 'NONE', ( #4694 ), #4071, .F. ) ;
#2576=CYLINDRICAL_SURFACE ( 'NONE', #2020, 4.250000000000000000 ) ;
#2591=CARTESIAN_POINT ( 'NONE',  ( 30.00000000000000000, 2.054999999999997939, -6.938893903907228378E-15 ) ) ;
#2606=PLANE ( 'NONE',  #6198 ) ;
#2607=( NAMED_UNIT ( * ) PLANE_ANGLE_UNIT ( ) SI_UNIT ( $, .RADIAN. ) );
#2650=CARTESIAN_POINT ( 'NONE',  ( 29.55500000000002458, 0.000000000000000000, -6.938893903907228378E-15 ) ) ;
#2660=DIRECTION ( 'NONE',  ( -1.000000000000000000, 0.000000000000000000, 0.000000000000000000 ) ) ;
#2665=EDGE_CURVE ( 'NONE', #244, #8139, #5751, .T. ) ;
#2693=CARTESIAN_POINT ( 'NONE',  ( 5.000000000000015099, 0.000000000000000000, 0.000000000000000000 ) ) ;
#2712=ORIENTED_EDGE ( 'NONE', *, *, #2492, .T. ) ;
#2717=CARTESIAN_POINT ( 'NONE',  ( -31.74999999999994316, 0.000000000000000000, 0.000000000000000000 ) ) ;
#2739=DIRECTION ( 'NONE',  ( 0.000000000000000000, 0.000000000000000000, 1.000000000000000000 ) ) ;
#2744=EDGE_CURVE ( 'NONE', #8139, #2810, #5988, .T. ) ;
#2751=AXIS2_PLACEMENT_3D ( 'NONE', #7856, #4705, #1546 ) ;
#2752=COLOUR_RGB ( '', 0.31764706, 0.68627451, 0.89019608) ;
#2756=EDGE_CURVE ( 'NONE', #2818, #2258, #3472, .T. ) ;
#2757=CARTESIAN_POINT ( 'NONE',  ( 5.000000000000015099, 0.000000000000000000, 0.000000000000000000 ) ) ;
#2760=FACE_OUTER_BOUND ( 'NONE', #7981, .T. ) ;
#2761=CLOSED_SHELL ( 'NONE', ( #4611, #3360, #6732, #971, #6074, #5441, #2830, #738, #105, #2406, #504, #7061, #2910, #7538, #8011, #3103, #1163, #5698, #2570, #2230, #2972, #2932, #1034, #5744, #4629, #1236, #2785 ) ) ;
#2762=AXIS2_PLACEMENT_3D ( 'NONE', #2693, #3279, #5854 ) ;
#2764=CONICAL_SURFACE ( 'NONE', #5948, 2.055000000000000160, 0.7853981633974717047 ) ;
#2767=DIRECTION ( 'NONE',  ( -1.000000000000000000, 0.000000000000000000, 0.000000000000000000 ) ) ;
#2785=ADVANCED_FACE ( 'NONE', ( #3658 ), #4196, .F. ) ;
#2790=PRODUCT_DEFINITION ( 'UNKNOWN', '', #5640, #7573 ) ;
#2802=EDGE_CURVE ( 'NONE', #3217, #4315, #3245, .T. ) ;
#2805=EDGE_CURVE ( 'NONE', #4315, #117, #733, .T. ) ;
#2809=EDGE_LOOP ( 'NONE', ( #5930, #3009, #681, #7461 ) ) ;
#2810=VERTEX_POINT ( 'NONE', #663 ) ;
#2818=VERTEX_POINT ( 'NONE', #6461 ) ;
#2823=DIRECTION ( 'NONE',  ( 0.000000000000000000, -0.5000000000000009992, -0.8660254037844380415 ) ) ;
#2826=CARTESIAN_POINT ( 'NONE',  ( 2.500000000000002220, -2.357898499370430834, 3.469446951953614189E-15 ) ) ;
#2830=ADVANCED_FACE ( 'NONE', ( #2072, #3280 ), #7095, .T. ) ;
#2831=VERTEX_POINT ( 'NONE', #5778 ) ;
#2832=EDGE_LOOP ( 'NONE', ( #2203, #6719, #3807, #7702, #7394 ) ) ;
#2834=LINE ( 'NONE', #5256, #6753 ) ;
#2843=AXIS2_PLACEMENT_3D ( 'NONE', #932, #6575, #3476 ) ;
#2878=DIRECTION ( 'NONE',  ( 0.000000000000000000, 0.000000000000000000, -1.000000000000000000 ) ) ;
#2892=DIRECTION ( 'NONE',  ( -1.000000000000000000, 0.000000000000000000, 0.000000000000000000 ) ) ;
#2898=EDGE_LOOP ( 'NONE', ( #1902, #1266, #2372 ) ) ;
#2910=ADVANCED_FACE ( 'NONE', ( #68 ), #8035, .F. ) ;
#2914=ORIENTED_EDGE ( 'NONE', *, *, #3294, .T. ) ;
#2924=VECTOR ( 'NONE', #1951, 1000.000000000000114 ) ;
#2927=CARTESIAN_POINT ( 'NONE',  ( 2.500000000000002220, 1.178949249685212086, -2.042000000000002036 ) ) ;
#2932=ADVANCED_FACE ( 'NONE', ( #4846 ), #344, .F. ) ;
#2936=PLANE ( 'NONE',  #205 ) ;
#2949=CARTESIAN_POINT ( 'NONE',  ( 0.000000000000000000, -2.357898499370430834, 3.469446951953614189E-15 ) ) ;
#2972=ADVANCED_FACE ( 'NONE', ( #6709 ), #2936, .F. ) ;
#2980=ORIENTED_EDGE ( 'NONE', *, *, #4924, .F. ) ;
#2986=EDGE_CURVE ( 'NONE', #117, #1235, #1525, .T. ) ;
#3003=PLANE ( 'NONE',  #6111 ) ;
#3007=EDGE_CURVE ( 'NONE', #6705, #4315, #7990, .T. ) ;
#3009=ORIENTED_EDGE ( 'NONE', *, *, #6153, .T. ) ;
#3010=( NAMED_UNIT ( * ) PLANE_ANGLE_UNIT ( ) SI_UNIT ( $, .RADIAN. ) );
#3016=AXIS2_PLACEMENT_3D ( 'NONE', #4805, #3477, #7370 ) ;
#3027=LINE ( 'NONE', #8098, #6203 ) ;
#3038=DIRECTION ( 'NONE',  ( 0.000000000000000000, 1.000000000000000000, -1.103561164596346103E-15 ) ) ;
#3040=DIRECTION ( 'NONE',  ( 0.000000000000000000, 0.000000000000000000, 1.000000000000000000 ) ) ;
#3043=ORIENTED_EDGE ( 'NONE', *, *, #2665, .F. ) ;
#3081=ORIENTED_EDGE ( 'NONE', *, *, #5141, .T. ) ;
#3084=VECTOR ( 'NONE', #1616, 1000.000000000000000 ) ;
#3103=ADVANCED_FACE ( 'NONE', ( #7591 ), #2606, .F. ) ;
#3176=CARTESIAN_POINT ( 'NONE',  ( 0.000000000000000000, -1.178949249685215417, 2.042000000000002036 ) ) ;
#3183=DIRECTION ( 'NONE',  ( 0.000000000000000000, 0.000000000000000000, -1.000000000000000000 ) ) ;
#3203=CARTESIAN_POINT ( 'NONE',  ( 2.500000000000002220, 1.178949249685212086, -2.042000000000002036 ) ) ;
#3214=ORIENTED_EDGE ( 'NONE', *, *, #3612, .F. ) ;
#3217=VERTEX_POINT ( 'NONE', #7662 ) ;
#3218=EDGE_LOOP ( 'NONE', ( #5927, #5692 ) ) ;
#3222=LINE ( 'NONE', #6858, #4366 ) ;
#3239=CARTESIAN_POINT ( 'NONE',  ( 5.000000000000015099, 0.000000000000000000, 4.250000000000000000 ) ) ;
#3245=LINE ( 'NONE', #1961, #3820 ) ;
#3266=CARTESIAN_POINT ( 'NONE',  ( 30.00000000000000000, 2.516649172247811061E-16, -2.055000000000006821 ) ) ;
#3275=EDGE_CURVE ( 'NONE', #4032, #4428, #250, .T. ) ;
#3277=ORIENTED_EDGE ( 'NONE', *, *, #1212, .F. ) ;
#3279=DIRECTION ( 'NONE',  ( -1.000000000000000000, 0.000000000000000000, 0.000000000000000000 ) ) ;
#3280=FACE_OUTER_BOUND ( 'NONE', #3603, .T. ) ;
#3294=EDGE_CURVE ( 'NONE', #1037, #2831, #7231, .T. ) ;
#3331=ORIENTED_EDGE ( 'NONE', *, *, #241, .F. ) ;
#3343=ORIENTED_EDGE ( 'NONE', *, *, #7645, .F. ) ;
#3349=FACE_OUTER_BOUND ( 'NONE', #7195, .T. ) ;
#3350=FACE_OUTER_BOUND ( 'NONE', #6063, .T. ) ;
#3356=ORIENTED_EDGE ( 'NONE', *, *, #5203, .T. ) ;
#3360=ADVANCED_FACE ( 'NONE', ( #204 ), #7256, .T. ) ;
#3374=ORIENTED_EDGE ( 'NONE', *, *, #7329, .F. ) ;
#3382=DIRECTION ( 'NONE',  ( 0.000000000000000000, 0.000000000000000000, 1.000000000000000000 ) ) ;
#3390=CARTESIAN_POINT ( 'NONE',  ( 0.2500000000000002220, 5.204748896376238866E-16, -4.249999999999979572 ) ) ;
#3405=DIRECTION ( 'NONE',  ( -1.000000000000000000, 0.000000000000000000, 0.000000000000000000 ) ) ;
#3411=ORIENTED_EDGE ( 'NONE', *, *, #6816, .F. ) ;
#3412=ORIENTED_EDGE ( 'NONE', *, *, #4924, .T. ) ;
#3414=CARTESIAN_POINT ( 'NONE',  ( 0.000000000000000000, 1.178949249685212086, -2.042000000000002036 ) ) ;
#3457=PRODUCT_CONTEXT ( 'NONE', #3487, 'mechanical' ) ;
#3466=VECTOR ( 'NONE', #2342, 1000.000000000000114 ) ;
#3472=CIRCLE ( 'NONE', #6267, 2.500000000000000444 ) ;
#3476=DIRECTION ( 'NONE',  ( 0.000000000000000000, 0.000000000000000000, -1.000000000000000000 ) ) ;
#3477=DIRECTION ( 'NONE',  ( -1.000000000000000000, 0.000000000000000000, 0.000000000000000000 ) ) ;
#3484=ORIENTED_EDGE ( 'NONE', *, *, #4027, .T. ) ;
#3487=APPLICATION_CONTEXT ( 'automotive_design' ) ;
#3488=EDGE_LOOP ( 'NONE', ( #3374, #3640, #3996, #5251 ) ) ;
#3521=CYLINDRICAL_SURFACE ( 'NONE', #7978, 2.500000000000000444 ) ;
#3531=AXIS2_PLACEMENT_3D ( 'NONE', #1725, #1088, #3632 ) ;
#3546=CARTESIAN_POINT ( 'NONE',  ( 5.000000000000018652, 0.000000000000000000, -2.700000000000004174 ) ) ;
#3557=CARTESIAN_POINT ( 'NONE',  ( 2.500000000000002220, 2.357898499370434386, -3.469446951953614189E-15 ) ) ;
#3559=DIRECTION ( 'NONE',  ( 0.000000000000000000, -1.224646799147353454E-16, 1.000000000000000000 ) ) ;
#3572=DIRECTION ( 'NONE',  ( 1.000000000000000000, 0.000000000000000000, 0.000000000000000000 ) ) ;
#3575=DIRECTION ( 'NONE',  ( 0.000000000000000000, -1.287488025362403787E-15, -1.000000000000000000 ) ) ;
#3576=PLANE ( 'NONE',  #8198 ) ;
#3587=DIRECTION ( 'NONE',  ( -1.000000000000000000, 0.000000000000000000, 0.000000000000000000 ) ) ;
#3588=CIRCLE ( 'NONE', #921, 0.2000000000000000944 ) ;
#3603=EDGE_LOOP ( 'NONE', ( #4497, #4414 ) ) ;
#3604=( LENGTH_UNIT ( ) NAMED_UNIT ( * ) SI_UNIT ( .MILLI., .METRE. ) );
#3612=EDGE_CURVE ( 'NONE', #4887, #6175, #3222, .T. ) ;
#3626=LINE ( 'NONE', #456, #5456 ) ;
#3629=EDGE_CURVE ( 'NONE', #5583, #6246, #4090, .T. ) ;
#3632=DIRECTION ( 'NONE',  ( 0.000000000000000000, 0.000000000000000000, 1.000000000000000000 ) ) ;
#3640=ORIENTED_EDGE ( 'NONE', *, *, #259, .F. ) ;
#3646=APPLICATION_CONTEXT ( 'automotive_design' ) ;
#3658=FACE_OUTER_BOUND ( 'NONE', #4575, .T. ) ;
#3667=LINE ( 'NONE', #494, #2252 ) ;
#3673=VERTEX_POINT ( 'NONE', #4422 ) ;
#3679=ORIENTED_EDGE ( 'NONE', *, *, #3612, .T. ) ;
#3689=ORIENTED_EDGE ( 'NONE', *, *, #8156, .T. ) ;
#3698=AXIS2_PLACEMENT_3D ( 'NONE', #1755, #2414, #6640 ) ;
#3709=ORIENTED_EDGE ( 'NONE', *, *, #4735, .T. ) ;
#3716=CIRCLE ( 'NONE', #5834, 0.2000000000000000944 ) ;
#3726=VECTOR ( 'NONE', #2139, 1000.000000000000000 ) ;
#3737=ORIENTED_EDGE ( 'NONE', *, *, #5651, .F. ) ;
#3738=PRESENTATION_STYLE_ASSIGNMENT (( #6167 ) ) ;
#3765=ORIENTED_EDGE ( 'NONE', *, *, #7645, .T. ) ;
#3768=ORIENTED_EDGE ( 'NONE', *, *, #6153, .F. ) ;
#3807=ORIENTED_EDGE ( 'NONE', *, *, #8141, .T. ) ;
#3815=SURFACE_SIDE_STYLE ('',( #4627 ) ) ;
#3820=VECTOR ( 'NONE', #7056, 1000.000000000000000 ) ;
#3823=DIRECTION ( 'NONE',  ( -1.000000000000000000, 0.000000000000000000, 0.000000000000000000 ) ) ;
#3842=ORIENTED_EDGE ( 'NONE', *, *, #2805, .F. ) ;
#3865=CARTESIAN_POINT ( 'NONE',  ( 5.200000000000020606, 3.306546357697854226E-16, 2.699999999999993516 ) ) ;
#3867=VECTOR ( 'NONE', #79, 1000.000000000000114 ) ;
#3889=ORIENTED_EDGE ( 'NONE', *, *, #7737, .F. ) ;
#3911=EDGE_CURVE ( 'NONE', #6759, #2831, #1441, .T. ) ;
#3942=CARTESIAN_POINT ( 'NONE',  ( 0.000000000000000000, 0.000000000000000000, 0.000000000000000000 ) ) ;
#3970=AXIS2_PLACEMENT_3D ( 'NONE', #5452, #989, #6058 ) ;
#3982=CARTESIAN_POINT ( 'NONE',  ( 2.500000000000002220, 2.357898499370434386, -3.469446951953614189E-15 ) ) ;
#3996=ORIENTED_EDGE ( 'NONE', *, *, #7737, .T. ) ;
#4000=AXIS2_PLACEMENT_3D ( 'NONE', #2650, #7779, #2065 ) ;
#4012=DIRECTION ( 'NONE',  ( 0.000000000000000000, -1.000000000000000000, 1.287488025362403787E-15 ) ) ;
#4027=EDGE_CURVE ( 'NONE', #1969, #992, #3027, .T. ) ;
#4028=CARTESIAN_POINT ( 'NONE',  ( 2.500000000000002220, 1.178949249685218970, 2.041999999999998483 ) ) ;
#4032=VERTEX_POINT ( 'NONE', #2454 ) ;
#4058=DIRECTION ( 'NONE',  ( 0.000000000000000000, 0.000000000000000000, -1.000000000000000000 ) ) ;
#4060=CARTESIAN_POINT ( 'NONE',  ( 0.2500000000000002220, 4.898587196589412829E-16, -3.999999999999979128 ) ) ;
#4062=DIRECTION ( 'NONE',  ( -1.000000000000000000, 0.000000000000000000, 0.000000000000000000 ) ) ;
#4071=PLANE ( 'NONE',  #1228 ) ;
#4083=CIRCLE ( 'NONE', #3016, 2.500000000000000888 ) ;
#4087=DIRECTION ( 'NONE',  ( 0.000000000000000000, 0.000000000000000000, 1.000000000000000000 ) ) ;
#4090=CIRCLE ( 'NONE', #1856, 2.055000000000000160 ) ;
#4095=AXIS2_PLACEMENT_3D ( 'NONE', #7802, #3405, #2739 ) ;
#4101=DIRECTION ( 'NONE',  ( -1.000000000000000000, 0.000000000000000000, 0.000000000000000000 ) ) ;
#4109=ORIENTED_EDGE ( 'NONE', *, *, #1541, .F. ) ;
#4113=CARTESIAN_POINT ( 'NONE',  ( 30.00000000000000000, 0.000000000000000000, -6.938893903907228378E-15 ) ) ;
#4153=CARTESIAN_POINT ( 'NONE',  ( 2.500000000000002220, 1.178949249685212086, -2.042000000000002036 ) ) ;
#4156=DIRECTION ( 'NONE',  ( 1.000000000000000000, -0.000000000000000000, -0.000000000000000000 ) ) ;
#4158=COLOUR_RGB ( '', 0.31764706, 0.68627451, 0.89019608) ;
#4196=CONICAL_SURFACE ( 'NONE', #5266, 2.041999999999999815, 1.047197551196591858 ) ;
#4251=TOROIDAL_SURFACE ( 'NONE', #670, 4.000000000000000000, 0.2500000000000000000 ) ;
#4268=FILL_AREA_STYLE_COLOUR ( '', #2752 ) ;
#4269=CARTESIAN_POINT ( 'NONE',  ( -31.74999999999994316, 0.000000000000000000, 0.000000000000000000 ) ) ;
#4287=ORIENTED_EDGE ( 'NONE', *, *, #753, .F. ) ;
#4315=VERTEX_POINT ( 'NONE', #524 ) ;
#4320=DIRECTION ( 'NONE',  ( 0.000000000000000000, 0.000000000000000000, -1.000000000000000000 ) ) ;
#4325=ORIENTED_EDGE ( 'NONE', *, *, #6735, .T. ) ;
#4346=SURFACE_STYLE_FILL_AREA ( #7463 ) ;
#4348=FACE_OUTER_BOUND ( 'NONE', #2832, .T. ) ;
#4361=CIRCLE ( 'NONE', #3970, 4.000000000000000000 ) ;
#4365=ORIENTED_EDGE ( 'NONE', *, *, #222, .T. ) ;
#4366=VECTOR ( 'NONE', #8106, 1000.000000000000000 ) ;
#4370=CIRCLE ( 'NONE', #2241, 0.2500000000000002220 ) ;
#4375=FACE_OUTER_BOUND ( 'NONE', #7841, .T. ) ;
#4414=ORIENTED_EDGE ( 'NONE', *, *, #5661, .T. ) ;
#4422=CARTESIAN_POINT ( 'NONE',  ( 2.500000000000002220, -2.357898499370430834, 3.469446951953614189E-15 ) ) ;
#4425=ORIENTED_EDGE ( 'NONE', *, *, #7826, .T. ) ;
#4428=VERTEX_POINT ( 'NONE', #5654 ) ;
#4429=DIRECTION ( 'NONE',  ( -0.7071067811865310304, 8.659560562355135004E-17, -0.7071067811865641151 ) ) ;
#4431=DIRECTION ( 'NONE',  ( 0.000000000000000000, 1.103561164596346103E-15, 1.000000000000000000 ) ) ;
#4459=LINE ( 'NONE', #3176, #3867 ) ;
#4474=AXIS2_PLACEMENT_3D ( 'NONE', #3557, #304, #887 ) ;
#4482=DIRECTION ( 'NONE',  ( 0.000000000000000000, 0.000000000000000000, 1.000000000000000000 ) ) ;
#4493=DIRECTION ( 'NONE',  ( 0.000000000000000000, 0.000000000000000000, -1.000000000000000000 ) ) ;
#4497=ORIENTED_EDGE ( 'NONE', *, *, #1582, .T. ) ;
#4533=DIRECTION ( 'NONE',  ( 0.000000000000000000, 0.000000000000000000, 1.000000000000000000 ) ) ;
#4550=ORIENTED_EDGE ( 'NONE', *, *, #4027, .F. ) ;
#4575=EDGE_LOOP ( 'NONE', ( #3277, #2526, #4325, #1089, #3709 ) ) ;
#4586=ORIENTED_EDGE ( 'NONE', *, *, #7483, .T. ) ;
#4590=FILL_AREA_STYLE ('',( #2568 ) ) ;
#4592=EDGE_CURVE ( 'NONE', #7111, #7104, #6217, .T. ) ;
#4603=PLANE ( 'NONE',  #2843 ) ;
#4611=ADVANCED_FACE ( 'NONE', ( #2263 ), #516, .F. ) ;
#4627=SURFACE_STYLE_FILL_AREA ( #4590 ) ;
#4629=ADVANCED_FACE ( 'NONE', ( #3349 ), #7281, .F. ) ;
#4642=DIRECTION ( 'NONE',  ( 0.000000000000000000, 0.000000000000000000, 1.000000000000000000 ) ) ;
#4680=CARTESIAN_POINT ( 'NONE',  ( 2.500000000000002220, 0.000000000000000000, 0.000000000000000000 ) ) ;
#4688=VERTEX_POINT ( 'NONE', #295 ) ;
#4694=FACE_OUTER_BOUND ( 'NONE', #1632, .T. ) ;
#4698=ORIENTED_EDGE ( 'NONE', *, *, #7483, .F. ) ;
#4701=CIRCLE ( 'NONE', #450, 2.500000000000000444 ) ;
#4705=DIRECTION ( 'NONE',  ( -1.000000000000000000, 0.000000000000000000, 0.000000000000000000 ) ) ;
#4735=EDGE_CURVE ( 'NONE', #1969, #244, #6364, .T. ) ;
#4748=CARTESIAN_POINT ( 'NONE',  ( 2.500000000000002220, 1.178949249685212086, -2.042000000000002036 ) ) ;
#4759=ORIENTED_EDGE ( 'NONE', *, *, #1541, .T. ) ;
#4771=VECTOR ( 'NONE', #6024, 1000.000000000000000 ) ;
#4786=EDGE_LOOP ( 'NONE', ( #6813, #1558, #5058 ) ) ;
#4805=CARTESIAN_POINT ( 'NONE',  ( 29.55500000000002458, 0.000000000000000000, -6.938893903907228378E-15 ) ) ;
#4806=CARTESIAN_POINT ( 'NONE',  ( 2.500000000000002220, 2.357898499370434386, -3.469446951953614189E-15 ) ) ;
#4811=CARTESIAN_POINT ( 'NONE',  ( -31.74999999999994316, 0.000000000000000000, 0.000000000000000000 ) ) ;
#4816=CARTESIAN_POINT ( 'NONE',  ( 2.500000000000002220, -3.469446951953614189E-15, -2.041999999999998483 ) ) ;
#4840=CARTESIAN_POINT ( 'NONE',  ( 2.500000000000002220, 2.500728763858895382E-16, -2.041999999999999815 ) ) ;
#4846=FACE_OUTER_BOUND ( 'NONE', #4786, .T. ) ;
#4870=LINE ( 'NONE', #8105, #6616 ) ;
#4873=UNCERTAINTY_MEASURE_WITH_UNIT (LENGTH_MEASURE( 1.000000000000000082E-05 ), #3604, 'distance_accuracy_value', 'NONE');
#4887=VERTEX_POINT ( 'NONE', #2564 ) ;
#4891=DIRECTION ( 'NONE',  ( 0.000000000000000000, 0.000000000000000000, 1.000000000000000000 ) ) ;
#4902=AXIS2_PLACEMENT_3D ( 'NONE', #6530, #7123, #4087 ) ;
#4904=CIRCLE ( 'NONE', #4000, 2.500000000000000888 ) ;
#4906=DIRECTION ( 'NONE',  ( 0.000000000000000000, -0.4999999999999992228, 0.8660254037844390407 ) ) ;
#4913=CIRCLE ( 'NONE', #8085, 2.055000000000000160 ) ;
#4924=EDGE_CURVE ( 'NONE', #5583, #7658, #2516, .T. ) ;
#4927=DIRECTION ( 'NONE',  ( -1.000000000000000000, 0.000000000000000000, 0.000000000000000000 ) ) ;
#4932=DIRECTION ( 'NONE',  ( -1.000000000000000000, 0.000000000000000000, 0.000000000000000000 ) ) ;
#4939=VERTEX_POINT ( 'NONE', #5064 ) ;
#4941=( NAMED_UNIT ( * ) SI_UNIT ( $, .STERADIAN. ) SOLID_ANGLE_UNIT ( ) );
#4948=VERTEX_POINT ( 'NONE', #7534 ) ;
#4957=ORIENTED_EDGE ( 'NONE', *, *, #7093, .T. ) ;
#4989=ORIENTED_EDGE ( 'NONE', *, *, #1212, .T. ) ;
#4993=DIRECTION ( 'NONE',  ( 0.000000000000000000, 0.000000000000000000, 1.000000000000000000 ) ) ;
#5009=ORIENTED_EDGE ( 'NONE', *, *, #5203, .F. ) ;
#5020=LINE ( 'NONE', #7504, #5696 ) ;
#5027=CARTESIAN_POINT ( 'NONE',  ( 2.500000000000002220, -1.178949249685215417, 2.042000000000002036 ) ) ;
#5028=EDGE_CURVE ( 'NONE', #4948, #6759, #2834, .T. ) ;
#5036=VECTOR ( 'NONE', #5367, 1000.000000000000000 ) ;
#5050=DIRECTION ( 'NONE',  ( 0.000000000000000000, 0.000000000000000000, 1.000000000000000000 ) ) ;
#5055=AXIS2_PLACEMENT_3D ( 'NONE', #2717, #5261, #6613 ) ;
#5058=ORIENTED_EDGE ( 'NONE', *, *, #2744, .F. ) ;
#5064=CARTESIAN_POINT ( 'NONE',  ( 0.000000000000000000, -1.178949249685215417, 2.042000000000002036 ) ) ;
#5073=AXIS2_PLACEMENT_3D ( 'NONE', #211, #257, #297 ) ;
#5079=DIRECTION ( 'NONE',  ( 0.000000000000000000, -0.8660254037844390407, -0.4999999999999992784 ) ) ;
#5087=DIRECTION ( 'NONE',  ( 1.000000000000000000, 0.000000000000000000, 0.000000000000000000 ) ) ;
#5088=PLANE ( 'NONE',  #1446 ) ;
#5091=ORIENTED_EDGE ( 'NONE', *, *, #5651, .T. ) ;
#5097=DIRECTION ( 'NONE',  ( 0.000000000000000000, 0.000000000000000000, 1.000000000000000000 ) ) ;
#5098=DIRECTION ( 'NONE',  ( 0.000000000000000000, -1.000000000000000000, 0.000000000000000000 ) ) ;
#5126=CARTESIAN_POINT ( 'NONE',  ( 0.000000000000000000, 0.000000000000000000, 0.000000000000000000 ) ) ;
#5130=ORIENTED_EDGE ( 'NONE', *, *, #5379, .T. ) ;
#5134=PRODUCT_DEFINITION_SHAPE ( 'NONE', 'NONE',  #2790 ) ;
#5135=CARTESIAN_POINT ( 'NONE',  ( 2.500000000000002220, 0.000000000000000000, 0.000000000000000000 ) ) ;
#5141=EDGE_CURVE ( 'NONE', #4428, #6175, #1474, .T. ) ;
#5152=DIRECTION ( 'NONE',  ( 0.000000000000000000, 0.000000000000000000, 1.000000000000000000 ) ) ;
#5169=ORIENTED_EDGE ( 'NONE', *, *, #7329, .T. ) ;
#5183=AXIS2_PLACEMENT_3D ( 'NONE', #2338, #4932, #2431 ) ;
#5203=EDGE_CURVE ( 'NONE', #3217, #2810, #4870, .T. ) ;
#5226=DIRECTION ( 'NONE',  ( 0.000000000000000000, -0.5000000000000011102, -0.8660254037844379305 ) ) ;
#5230=LINE ( 'NONE', #3982, #2924 ) ;
#5237=FACE_BOUND ( 'NONE', #1295, .T. ) ;
#5251=ORIENTED_EDGE ( 'NONE', *, *, #4592, .F. ) ;
#5256=CARTESIAN_POINT ( 'NONE',  ( -31.74999999999994316, 5.204748896376250699E-16, -4.250000000000000000 ) ) ;
#5260=CARTESIAN_POINT ( 'NONE',  ( 2.500000000000002220, 2.357898499370434386, -3.469446951953614189E-15 ) ) ;
#5261=DIRECTION ( 'NONE',  ( -1.000000000000000000, 0.000000000000000000, 0.000000000000000000 ) ) ;
#5262=AXIS2_PLACEMENT_3D ( 'NONE', #1414, #7530, #3183 ) ;
#5263=CARTESIAN_POINT ( 'NONE',  ( 2.500000000000015987, -1.768423874527823347, -1.020999999999997687 ) ) ;
#5266=AXIS2_PLACEMENT_3D ( 'NONE', #5811, #2040, #5855 ) ;
#5272=DIRECTION ( 'NONE',  ( 1.000000000000000000, 0.000000000000000000, 0.000000000000000000 ) ) ;
#5273=EDGE_CURVE ( 'NONE', #4939, #1235, #3667, .T. ) ;
#5275=EDGE_CURVE ( 'NONE', #5642, #6175, #5586, .T. ) ;
#5280=EDGE_LOOP ( 'NONE', ( #2980, #1808, #4586, #1571 ) ) ;
#5297=EDGE_LOOP ( 'NONE', ( #8007, #1203, #3842, #75, #182 ) ) ;
#5299=VECTOR ( 'NONE', #2823, 1000.000000000000114 ) ;
#5304=CARTESIAN_POINT ( 'NONE',  ( 30.00000000000000000, 0.000000000000000000, -6.938893903907228378E-15 ) ) ;
#5305=VECTOR ( 'NONE', #5563, 1000.000000000000000 ) ;
#5359=LINE ( 'NONE', #1493, #3084 ) ;
#5363=ORIENTED_EDGE ( 'NONE', *, *, #241, .T. ) ;
#5367=DIRECTION ( 'NONE',  ( 0.000000000000000000, 0.4999999999999991118, -0.8660254037844391517 ) ) ;
#5379=EDGE_CURVE ( 'NONE', #2810, #4315, #8066, .T. ) ;
#5391=DIRECTION ( 'NONE',  ( 1.000000000000000000, 0.000000000000000000, 0.000000000000000000 ) ) ;
#5400=ORIENTED_EDGE ( 'NONE', *, *, #551, .F. ) ;
#5416=CIRCLE ( 'NONE', #359, 2.041999999999999815 ) ;
#5422=CARTESIAN_POINT ( 'NONE',  ( 5.000000000000018652, 3.306546357697858171E-16, 2.699999999999997069 ) ) ;
#5441=ADVANCED_FACE ( 'NONE', ( #4375 ), #2764, .T. ) ;
#5445=EDGE_CURVE ( 'NONE', #8139, #4887, #1463, .T. ) ;
#5452=CARTESIAN_POINT ( 'NONE',  ( 0.000000000000000000, 0.000000000000000000, 0.000000000000000000 ) ) ;
#5456=VECTOR ( 'NONE', #6149, 1000.000000000000114 ) ;
#5473=CARTESIAN_POINT ( 'NONE',  ( 0.000000000000000000, 1.178949249685218970, 2.041999999999998483 ) ) ;
#5488=ORIENTED_EDGE ( 'NONE', *, *, #3911, .T. ) ;
#5491=CARTESIAN_POINT ( 'NONE',  ( 2.500000000000002220, 2.357898499370434386, -3.469446951953614189E-15 ) ) ;
#5508=EDGE_LOOP ( 'NONE', ( #1633, #8028, #5488, #7972 ) ) ;
#5528=EDGE_CURVE ( 'NONE', #4948, #1037, #7141, .T. ) ;
#5552=FACE_OUTER_BOUND ( 'NONE', #6054, .T. ) ;
#5563=DIRECTION ( 'NONE',  ( -1.000000000000000000, 0.000000000000000000, 0.000000000000000000 ) ) ;
#5583=VERTEX_POINT ( 'NONE', #2326 ) ;
#5586=LINE ( 'NONE', #7317, #4771 ) ;
#5613=CARTESIAN_POINT ( 'NONE',  ( 2.500000000000002220, -2.357898499370430834, 3.469446951953614189E-15 ) ) ;
#5640=PRODUCT_DEFINITION_FORMATION_WITH_SPECIFIED_SOURCE ( 'ANY', '', #8089, .NOT_KNOWN. ) ;
#5642=VERTEX_POINT ( 'NONE', #2949 ) ;
#5651=EDGE_CURVE ( 'NONE', #2831, #6759, #6875, .T. ) ;
#5654=CARTESIAN_POINT ( 'NONE',  ( 0.000000000000000000, 1.178949249685212086, -2.042000000000002036 ) ) ;
#5661=EDGE_CURVE ( 'NONE', #1110, #8109, #4361, .T. ) ;
#5666=CIRCLE ( 'NONE', #5262, 2.700000000000000622 ) ;
#5672=VECTOR ( 'NONE', #2109, 1000.000000000000000 ) ;
#5686=CARTESIAN_POINT ( 'NONE',  ( 0.000000000000000000, 0.000000000000000000, 4.000000000000000000 ) ) ;
#5688=DIRECTION ( 'NONE',  ( 0.000000000000000000, 0.000000000000000000, -1.000000000000000000 ) ) ;
#5692=ORIENTED_EDGE ( 'NONE', *, *, #3629, .F. ) ;
#5696=VECTOR ( 'NONE', #3823, 1000.000000000000000 ) ;
#5698=ADVANCED_FACE ( 'NONE', ( #1029 ), #3576, .T. ) ;
#5725=( NAMED_UNIT ( * ) SI_UNIT ( $, .STERADIAN. ) SOLID_ANGLE_UNIT ( ) );
#5744=ADVANCED_FACE ( 'NONE', ( #6313 ), #5088, .F. ) ;
#5751=CIRCLE ( 'NONE', #8115, 2.041999999999999815 ) ;
#5764=DIRECTION ( 'NONE',  ( 0.000000000000000000, -1.000000000000000000, 1.103561164596346103E-15 ) ) ;
#5778=CARTESIAN_POINT ( 'NONE',  ( 0.2500000000000002220, 0.000000000000000000, 4.250000000000021316 ) ) ;
#5779=DIRECTION ( 'NONE',  ( 1.000000000000000000, 0.000000000000000000, 0.000000000000000000 ) ) ;
#5797=CARTESIAN_POINT ( 'NONE',  ( 2.500000000000002220, -1.178949249685215417, 2.042000000000002036 ) ) ;
#5798=SURFACE_STYLE_USAGE ( .BOTH. , #3815 ) ;
#5811=CARTESIAN_POINT ( 'NONE',  ( 2.500000000000002220, 0.000000000000000000, 0.000000000000000000 ) ) ;
#5823=CARTESIAN_POINT ( 'NONE',  ( 29.55500000000002458, 3.061616997868375746E-16, -2.500000000000000888 ) ) ;
#5827=CIRCLE ( 'NONE', #2762, 4.250000000000000000 ) ;
#5834=AXIS2_PLACEMENT_3D ( 'NONE', #3865, #7086, #5881 ) ;
#5850=PLANE ( 'NONE',  #928 ) ;
#5854=DIRECTION ( 'NONE',  ( 0.000000000000000000, 0.000000000000000000, 1.000000000000000000 ) ) ;
#5855=DIRECTION ( 'NONE',  ( 0.000000000000000000, 0.000000000000000000, 1.000000000000000000 ) ) ;
#5880=CYLINDRICAL_SURFACE ( 'NONE', #5055, 4.250000000000000000 ) ;
#5881=DIRECTION ( 'NONE',  ( 0.000000000000000000, 1.224646799147353207E-16, 1.000000000000000000 ) ) ;
#5914=CIRCLE ( 'NONE', #3531, 4.000000000000000000 ) ;
#5919=AXIS2_PLACEMENT_3D ( 'NONE', #2007, #5272, #1410 ) ;
#5921=CARTESIAN_POINT ( 'NONE',  ( 2.500000000000002220, 0.000000000000000000, 0.000000000000000000 ) ) ;
#5926=CARTESIAN_POINT ( 'NONE',  ( 2.500000000000002220, 2.357898499370434386, -3.469446951953614189E-15 ) ) ;
#5927=ORIENTED_EDGE ( 'NONE', *, *, #7157, .F. ) ;
#5930=ORIENTED_EDGE ( 'NONE', *, *, #6816, .T. ) ;
#5944=DIRECTION ( 'NONE',  ( -1.000000000000000000, 0.000000000000000000, 0.000000000000000000 ) ) ;
#5948=AXIS2_PLACEMENT_3D ( 'NONE', #6281, #6946, #5050 ) ;
#5951=AXIS2_PLACEMENT_3D ( 'NONE', #567, #5079, #6213 ) ;
#5954=DIRECTION ( 'NONE',  ( 0.000000000000000000, -1.000000000000000000, 1.287488025362403787E-15 ) ) ;
#5975=CARTESIAN_POINT ( 'NONE',  ( 2.500000000000002220, 1.178949249685218970, 2.041999999999998483 ) ) ;
#5981=SHAPE_DEFINITION_REPRESENTATION ( #5134, #499 ) ;
#5988=CIRCLE ( 'NONE', #7059, 2.041999999999999815 ) ;
#6000=FACE_OUTER_BOUND ( 'NONE', #1213, .T. ) ;
#6006=( GEOMETRIC_REPRESENTATION_CONTEXT ( 3 ) GLOBAL_UNCERTAINTY_ASSIGNED_CONTEXT ( ( #459 ) ) GLOBAL_UNIT_ASSIGNED_CONTEXT ( ( #722, #1360, #5725 ) ) REPRESENTATION_CONTEXT ( 'NONE', 'WORKASPACE' ) );
#6024=DIRECTION ( 'NONE',  ( 0.000000000000000000, 0.4999999999999991118, -0.8660254037844391517 ) ) ;
#6029=DIRECTION ( 'NONE',  ( 1.000000000000000000, 0.000000000000000000, 0.000000000000000000 ) ) ;
#6054=EDGE_LOOP ( 'NONE', ( #1728, #7292, #4550, #7321, #1724 ) ) ;
#6058=DIRECTION ( 'NONE',  ( 0.000000000000000000, 0.000000000000000000, 1.000000000000000000 ) ) ;
#6063=EDGE_LOOP ( 'NONE', ( #200, #7026, #2914, #5091 ) ) ;
#6074=ADVANCED_FACE ( 'NONE', ( #6710 ), #345, .T. ) ;
#6088=CARTESIAN_POINT ( 'NONE',  ( 2.500000000000002220, 0.000000000000000000, 2.041999999999999815 ) ) ;
#6105=CARTESIAN_POINT ( 'NONE',  ( 2.500000000000002220, -2.357898499370430834, 3.469446951953614189E-15 ) ) ;
#6106=DIRECTION ( 'NONE',  ( 0.000000000000000000, 0.000000000000000000, 1.000000000000000000 ) ) ;
#6111=AXIS2_PLACEMENT_3D ( 'NONE', #1010, #7411, #6702 ) ;
#6136=LINE ( 'NONE', #8036, #8174 ) ;
#6141=DIRECTION ( 'NONE',  ( 0.000000000000000000, 0.000000000000000000, -1.000000000000000000 ) ) ;
#6149=DIRECTION ( 'NONE',  ( -0.7071067811865310304, 0.000000000000000000, 0.7071067811865641151 ) ) ;
#6151=ADVANCED_BREP_SHAPE_REPRESENTATION ( '', ( #6901, #1587 ), #6006 ) ;
#6153=EDGE_CURVE ( 'NONE', #7658, #2258, #5020, .T. ) ;
#6167=SURFACE_STYLE_USAGE ( .BOTH. , #7503 ) ;
#6175=VERTEX_POINT ( 'NONE', #6879 ) ;
#6179=CARTESIAN_POINT ( 'NONE',  ( 2.500000000000002220, 0.000000000000000000, 0.000000000000000000 ) ) ;
#6194=EDGE_LOOP ( 'NONE', ( #3768, #3689, #1698, #1819 ) ) ;
#6195=CARTESIAN_POINT ( 'NONE',  ( 2.500000000000002220, -2.357898499370430834, 3.469446951953614189E-15 ) ) ;
#6196=EDGE_LOOP ( 'NONE', ( #3484, #6811, #7331 ) ) ;
#6198=AXIS2_PLACEMENT_3D ( 'NONE', #5797, #4431, #5764 ) ;
#6203=VECTOR ( 'NONE', #8137, 1000.000000000000114 ) ;
#6205=DIRECTION ( 'NONE',  ( 0.000000000000000000, 0.5000000000000011102, 0.8660254037844380415 ) ) ;
#6213=DIRECTION ( 'NONE',  ( 0.000000000000000000, 0.4999999999999992784, -0.8660254037844390407 ) ) ;
#6217=CIRCLE ( 'NONE', #7147, 2.700000000000000622 ) ;
#6220=DIRECTION ( 'NONE',  ( 0.000000000000000000, -0.4999999999999992228, 0.8660254037844390407 ) ) ;
#6246=VERTEX_POINT ( 'NONE', #649 ) ;
#6254=LINE ( 'NONE', #4840, #3466 ) ;
#6257=EDGE_LOOP ( 'NONE', ( #7442, #1087, #3765, #7596, #86, #1977 ) ) ;
#6267=AXIS2_PLACEMENT_3D ( 'NONE', #2544, #5087, #6141 ) ;
#6273=AXIS2_PLACEMENT_3D ( 'NONE', #1139, #6748, #6205 ) ;
#6281=CARTESIAN_POINT ( 'NONE',  ( 30.00000000000000000, 0.000000000000000000, -6.938893903907228378E-15 ) ) ;
#6313=FACE_OUTER_BOUND ( 'NONE', #2898, .T. ) ;
#6329=AXIS2_PLACEMENT_3D ( 'NONE', #5126, #2660, #4533 ) ;
#6346=VECTOR ( 'NONE', #7296, 1000.000000000000114 ) ;
#6347=CARTESIAN_POINT ( 'NONE',  ( 2.500000000000002220, 2.357898499370434386, -3.469446951953614189E-15 ) ) ;
#6364=CIRCLE ( 'NONE', #5183, 2.041999999999999815 ) ;
#6373=EDGE_CURVE ( 'NONE', #2810, #3673, #317, .T. ) ;
#6378=VERTEX_POINT ( 'NONE', #5491 ) ;
#6384=SHAPE_REPRESENTATION_RELATIONSHIP ( 'NONE' , 'NONE' ,  #499, #6151 ) ;
#6439=ORIENTED_EDGE ( 'NONE', *, *, #6648, .F. ) ;
#6454=DIRECTION ( 'NONE',  ( 1.000000000000000000, 0.000000000000000000, 0.000000000000000000 ) ) ;
#6456=DIRECTION ( 'NONE',  ( 1.000000000000000000, 0.000000000000000000, 0.000000000000000000 ) ) ;
#6461=CARTESIAN_POINT ( 'NONE',  ( 5.200000000000020606, 0.000000000000000000, 2.499999999999993339 ) ) ;
#6465=AXIS2_PLACEMENT_3D ( 'NONE', #1523, #7903, #2145 ) ;
#6529=FACE_OUTER_BOUND ( 'NONE', #5508, .T. ) ;
#6530=CARTESIAN_POINT ( 'NONE',  ( 2.500000000000002220, 0.000000000000000000, 0.000000000000000000 ) ) ;
#6533=DIRECTION ( 'NONE',  ( -1.000000000000000000, 0.000000000000000000, 0.000000000000000000 ) ) ;
#6546=ORIENTED_EDGE ( 'NONE', *, *, #7157, .T. ) ;
#6575=DIRECTION ( 'NONE',  ( 1.000000000000000000, 0.000000000000000000, 0.000000000000000000 ) ) ;
#6576=FACE_OUTER_BOUND ( 'NONE', #709, .T. ) ;
#6588=DIRECTION ( 'NONE',  ( 0.000000000000000000, 1.000000000000000000, -1.287488025362403787E-15 ) ) ;
#6591=EDGE_CURVE ( 'NONE', #4032, #1235, #1288, .T. ) ;
#6609=CONICAL_SURFACE ( 'NONE', #901, 2.055000000000000160, 0.7853981633974717047 ) ;
#6613=DIRECTION ( 'NONE',  ( 0.000000000000000000, 0.000000000000000000, 1.000000000000000000 ) ) ;
#6616=VECTOR ( 'NONE', #1803, 1000.000000000000114 ) ;
#6631=DIRECTION ( 'NONE',  ( 0.000000000000000000, 0.000000000000000000, 1.000000000000000000 ) ) ;
#6637=DIRECTION ( 'NONE',  ( -1.000000000000000000, 0.000000000000000000, 0.000000000000000000 ) ) ;
#6640=DIRECTION ( 'NONE',  ( 0.000000000000000000, 0.000000000000000000, 1.000000000000000000 ) ) ;
#6648=EDGE_CURVE ( 'NONE', #1037, #4948, #5827, .T. ) ;
#6702=DIRECTION ( 'NONE',  ( 0.000000000000000000, 0.000000000000000000, -1.000000000000000000 ) ) ;
#6704=ORIENTED_EDGE ( 'NONE', *, *, #2665, .T. ) ;
#6705=VERTEX_POINT ( 'NONE', #933 ) ;
#6706=VECTOR ( 'NONE', #7757, 1000.000000000000000 ) ;
#6709=FACE_OUTER_BOUND ( 'NONE', #7187, .T. ) ;
#6710=FACE_OUTER_BOUND ( 'NONE', #2809, .T. ) ;
#6719=ORIENTED_EDGE ( 'NONE', *, *, #2446, .F. ) ;
#6732=ADVANCED_FACE ( 'NONE', ( #6576 ), #7001, .F. ) ;
#6735=EDGE_CURVE ( 'NONE', #4315, #4688, #5416, .T. ) ;
#6748=DIRECTION ( 'NONE',  ( 0.000000000000000000, 0.8660254037844380415, -0.5000000000000011102 ) ) ;
#6753=VECTOR ( 'NONE', #5944, 1000.000000000000000 ) ;
#6759=VERTEX_POINT ( 'NONE', #3390 ) ;
#6776=ORIENTED_EDGE ( 'NONE', *, *, #3007, .F. ) ;
#6802=ORIENTED_EDGE ( 'NONE', *, *, #7163, .T. ) ;
#6811=ORIENTED_EDGE ( 'NONE', *, *, #1635, .T. ) ;
#6813=ORIENTED_EDGE ( 'NONE', *, *, #222, .F. ) ;
#6816=EDGE_CURVE ( 'NONE', #6819, #7658, #4083, .T. ) ;
#6819=VERTEX_POINT ( 'NONE', #2309 ) ;
#6858=CARTESIAN_POINT ( 'NONE',  ( 2.500000000000002220, -1.178949249685218970, -2.041999999999998483 ) ) ;
#6875=CIRCLE ( 'NONE', #3698, 4.250000000000000000 ) ;
#6879=CARTESIAN_POINT ( 'NONE',  ( 0.000000000000000000, -1.178949249685218970, -2.041999999999998483 ) ) ;
#6885=AXIS2_PLACEMENT_3D ( 'NONE', #8040, #356, #2282 ) ;
#6892=DIRECTION ( 'NONE',  ( -1.000000000000000000, 0.000000000000000000, 0.000000000000000000 ) ) ;
#6901=MANIFOLD_SOLID_BREP ( 'Hex', #2761 ) ;
#6922=CARTESIAN_POINT ( 'NONE',  ( 5.200000000000020606, 3.061616997868392016E-16, -2.500000000000007994 ) ) ;
#6940=ORIENTED_EDGE ( 'NONE', *, *, #5445, .T. ) ;
#6946=DIRECTION ( 'NONE',  ( -1.000000000000000000, 0.000000000000000000, 0.000000000000000000 ) ) ;
#6961=ORIENTED_EDGE ( 'NONE', *, *, #1582, .F. ) ;
#7001=TOROIDAL_SURFACE ( 'NONE', #6465, 2.700000000000000622, 0.2000000000000000111 ) ;
#7026=ORIENTED_EDGE ( 'NONE', *, *, #5528, .T. ) ;
#7030=CARTESIAN_POINT ( 'NONE',  ( 30.00000000000000000, 0.000000000000000000, -6.938893903907228378E-15 ) ) ;
#7031=VECTOR ( 'NONE', #4429, 1000.000000000000114 ) ;
#7056=DIRECTION ( 'NONE',  ( 0.000000000000000000, 1.000000000000000000, -1.103561164596346103E-15 ) ) ;
#7059=AXIS2_PLACEMENT_3D ( 'NONE', #1882, #6892, #1207 ) ;
#7061=ADVANCED_FACE ( 'NONE', ( #3350 ), #5880, .T. ) ;
#7067=ORIENTED_EDGE ( 'NONE', *, *, #3911, .F. ) ;
#7086=DIRECTION ( 'NONE',  ( 0.000000000000000000, 1.000000000000000000, -1.224646799147353207E-16 ) ) ;
#7093=EDGE_CURVE ( 'NONE', #992, #4428, #380, .T. ) ;
#7095=PLANE ( 'NONE',  #6329 ) ;
#7104=VERTEX_POINT ( 'NONE', #3546 ) ;
#7105=ORIENTED_EDGE ( 'NONE', *, *, #4592, .T. ) ;
#7111=VERTEX_POINT ( 'NONE', #5422 ) ;
#7123=DIRECTION ( 'NONE',  ( -1.000000000000000000, 0.000000000000000000, 0.000000000000000000 ) ) ;
#7136=UNCERTAINTY_MEASURE_WITH_UNIT (LENGTH_MEASURE( 1.000000000000000082E-05 ), #21, 'distance_accuracy_value', 'NONE');
#7138=ORIENTED_EDGE ( 'NONE', *, *, #5275, .F. ) ;
#7141=CIRCLE ( 'NONE', #4095, 4.250000000000000000 ) ;
#7146=VECTOR ( 'NONE', #4906, 1000.000000000000114 ) ;
#7147=AXIS2_PLACEMENT_3D ( 'NONE', #2757, #1549, #2878 ) ;
#7155=VECTOR ( 'NONE', #5954, 1000.000000000000000 ) ;
#7157=EDGE_CURVE ( 'NONE', #6246, #5583, #4913, .T. ) ;
#7163=EDGE_CURVE ( 'NONE', #244, #4887, #7861, .T. ) ;
#7187=EDGE_LOOP ( 'NONE', ( #6802, #8102, #3043 ) ) ;
#7195=EDGE_LOOP ( 'NONE', ( #7306, #2712, #5400 ) ) ;
#7214=LINE ( 'NONE', #5926, #1492 ) ;
#7217=AXIS2_PLACEMENT_3D ( 'NONE', #5921, #7784, #4642 ) ;
#7231=LINE ( 'NONE', #7773, #1157 ) ;
#7256=TOROIDAL_SURFACE ( 'NONE', #2751, 4.000000000000000000, 0.2500000000000000000 ) ;
#7281=PLANE ( 'NONE',  #653 ) ;
#7292=ORIENTED_EDGE ( 'NONE', *, *, #7093, .F. ) ;
#7296=DIRECTION ( 'NONE',  ( -0.5000000000000051070, 0.000000000000000000, 0.8660254037844355990 ) ) ;
#7306=ORIENTED_EDGE ( 'NONE', *, *, #8141, .F. ) ;
#7317=CARTESIAN_POINT ( 'NONE',  ( 0.000000000000000000, -2.357898499370430834, 3.469446951953614189E-15 ) ) ;
#7321=ORIENTED_EDGE ( 'NONE', *, *, #2492, .F. ) ;
#7329=EDGE_CURVE ( 'NONE', #2818, #7111, #3716, .T. ) ;
#7331=ORIENTED_EDGE ( 'NONE', *, *, #4735, .F. ) ;
#7370=DIRECTION ( 'NONE',  ( 0.000000000000000000, 0.000000000000000000, 1.000000000000000000 ) ) ;
#7394=ORIENTED_EDGE ( 'NONE', *, *, #2986, .T. ) ;
#7411=DIRECTION ( 'NONE',  ( 1.000000000000000000, 0.000000000000000000, 0.000000000000000000 ) ) ;
#7417=ORIENTED_EDGE ( 'NONE', *, *, #5661, .F. ) ;
#7430=DIRECTION ( 'NONE',  ( 0.000000000000000000, 0.000000000000000000, -1.000000000000000000 ) ) ;
#7442=ORIENTED_EDGE ( 'NONE', *, *, #6591, .T. ) ;
#7461=ORIENTED_EDGE ( 'NONE', *, *, #1058, .F. ) ;
#7463=FILL_AREA_STYLE ('',( #4268 ) ) ;
#7477=DIRECTION ( 'NONE',  ( -1.000000000000000000, 0.000000000000000000, 0.000000000000000000 ) ) ;
#7478=STYLED_ITEM ( 'NONE', ( #1434 ), #6151 ) ;
#7483=EDGE_CURVE ( 'NONE', #6246, #6819, #3626, .T. ) ;
#7503=SURFACE_SIDE_STYLE ('',( #4346 ) ) ;
#7504=CARTESIAN_POINT ( 'NONE',  ( -31.74999999999994316, 3.061616997868383634E-16, -2.500000000000000444 ) ) ;
#7510=LINE ( 'NONE', #5613, #1182 ) ;
#7530=DIRECTION ( 'NONE',  ( -1.000000000000000000, -0.000000000000000000, -0.000000000000000000 ) ) ;
#7534=CARTESIAN_POINT ( 'NONE',  ( 5.000000000000015099, 5.204748896376250699E-16, -4.250000000000000000 ) ) ;
#7537=MECHANICAL_DESIGN_GEOMETRIC_PRESENTATION_REPRESENTATION('',(#1437),#1976);
#7538=ADVANCED_FACE ( 'NONE', ( #2463 ), #4251, .T. ) ;
#7544=AXIS2_PLACEMENT_3D ( 'NONE', #5135, #78, #5097 ) ;
#7570=ORIENTED_EDGE ( 'NONE', *, *, #2756, .F. ) ;
#7573=PRODUCT_DEFINITION_CONTEXT ( 'detailed design', #3646, 'design' ) ;
#7584=LINE ( 'NONE', #190, #6706 ) ;
#7591=FACE_OUTER_BOUND ( 'NONE', #5297, .T. ) ;
#7596=ORIENTED_EDGE ( 'NONE', *, *, #5275, .T. ) ;
#7614=FACE_OUTER_BOUND ( 'NONE', #3218, .T. ) ;
#7618=DIRECTION ( 'NONE',  ( 0.000000000000000000, 0.000000000000000000, -1.000000000000000000 ) ) ;
#7620=ORIENTED_EDGE ( 'NONE', *, *, #7826, .F. ) ;
#7645=EDGE_CURVE ( 'NONE', #4939, #5642, #4459, .T. ) ;
#7658=VERTEX_POINT ( 'NONE', #5823 ) ;
#7662=CARTESIAN_POINT ( 'NONE',  ( 2.500000000000002220, -1.178949249685215417, 2.042000000000002036 ) ) ;
#7669=AXIS2_PLACEMENT_3D ( 'NONE', #7970, #4156, #6106 ) ;
#7671=AXIS2_PLACEMENT_3D ( 'NONE', #4269, #2892, #4891 ) ;
#7702=ORIENTED_EDGE ( 'NONE', *, *, #1957, .T. ) ;
#7737=EDGE_CURVE ( 'NONE', #2258, #7104, #3588, .T. ) ;
#7750=CIRCLE ( 'NONE', #7217, 2.041999999999999815 ) ;
#7757=DIRECTION ( 'NONE',  ( 0.000000000000000000, -1.000000000000000000, 1.287488025362403787E-15 ) ) ;
#7773=CARTESIAN_POINT ( 'NONE',  ( -31.74999999999994316, 0.000000000000000000, 4.250000000000000000 ) ) ;
#7779=DIRECTION ( 'NONE',  ( -1.000000000000000000, 0.000000000000000000, 0.000000000000000000 ) ) ;
#7780=CARTESIAN_POINT ( 'NONE',  ( -31.74999999999994316, 0.000000000000000000, 2.500000000000000444 ) ) ;
#7784=DIRECTION ( 'NONE',  ( -1.000000000000000000, 0.000000000000000000, 0.000000000000000000 ) ) ;
#7796=ORIENTED_EDGE ( 'NONE', *, *, #1655, .F. ) ;
#7802=CARTESIAN_POINT ( 'NONE',  ( 5.000000000000015099, 0.000000000000000000, 0.000000000000000000 ) ) ;
#7826=EDGE_CURVE ( 'NONE', #6759, #1110, #4370, .T. ) ;
#7841=EDGE_LOOP ( 'NONE', ( #6546, #3412, #3411, #4698 ) ) ;
#7856=CARTESIAN_POINT ( 'NONE',  ( 0.2500000000000002220, 0.000000000000000000, 2.081668171172168513E-14 ) ) ;
#7861=LINE ( 'NONE', #4748, #7155 ) ;
#7903=DIRECTION ( 'NONE',  ( 1.000000000000000000, 0.000000000000000000, 0.000000000000000000 ) ) ;
#7925=ORIENTED_EDGE ( 'NONE', *, *, #1655, .T. ) ;
#7953=DIRECTION ( 'NONE',  ( 0.000000000000000000, 0.000000000000000000, 1.000000000000000000 ) ) ;
#7962=ORIENTED_EDGE ( 'NONE', *, *, #5528, .F. ) ;
#7970=CARTESIAN_POINT ( 'NONE',  ( 0.2500000000000002220, 0.000000000000000000, 2.081668171172168513E-14 ) ) ;
#7972=ORIENTED_EDGE ( 'NONE', *, *, #3294, .F. ) ;
#7978=AXIS2_PLACEMENT_3D ( 'NONE', #4811, #4062, #6631 ) ;
#7981=EDGE_LOOP ( 'NONE', ( #3343, #4287, #3356, #822, #4759 ) ) ;
#7990=LINE ( 'NONE', #6088, #6346 ) ;
#8007=ORIENTED_EDGE ( 'NONE', *, *, #5273, .T. ) ;
#8011=ADVANCED_FACE ( 'NONE', ( #4348 ), #1779, .T. ) ;
#8028=ORIENTED_EDGE ( 'NONE', *, *, #5028, .T. ) ;
#8035=TOROIDAL_SURFACE ( 'NONE', #5919, 2.700000000000000622, 0.2000000000000000111 ) ;
#8036=CARTESIAN_POINT ( 'NONE',  ( 2.500000000000002220, 2.357898499370434386, -3.469446951953614189E-15 ) ) ;
#8040=CARTESIAN_POINT ( 'NONE',  ( 0.2500000000000002220, 0.000000000000000000, 4.000000000000021316 ) ) ;
#8066=CIRCLE ( 'NONE', #7544, 2.041999999999999815 ) ;
#8085=AXIS2_PLACEMENT_3D ( 'NONE', #5304, #924, #3382 ) ;
#8089=PRODUCT ( 'socket head cap screw_iso_ISO 4762 M5 x 25 - 25N', 'socket head cap screw_iso_ISO 4762 M5 x 25 - 25N', '', ( #3457 ) ) ;
#8098=CARTESIAN_POINT ( 'NONE',  ( 2.500000000000002220, 2.357898499370434386, -3.469446951953614189E-15 ) ) ;
#8102=ORIENTED_EDGE ( 'NONE', *, *, #5445, .F. ) ;
#8105=CARTESIAN_POINT ( 'NONE',  ( 2.500000000000002220, -1.178949249685215417, 2.042000000000002036 ) ) ;
#8106=DIRECTION ( 'NONE',  ( -1.000000000000000000, 0.000000000000000000, 0.000000000000000000 ) ) ;
#8109=VERTEX_POINT ( 'NONE', #5686 ) ;
#8115=AXIS2_PLACEMENT_3D ( 'NONE', #6179, #7477, #4993 ) ;
#8128=LINE ( 'NONE', #5027, #5305 ) ;
#8132=DIRECTION ( 'NONE',  ( 0.000000000000000000, 0.4999999999999991118, -0.8660254037844391517 ) ) ;
#8137=DIRECTION ( 'NONE',  ( 0.000000000000000000, -0.5000000000000011102, -0.8660254037844379305 ) ) ;
#8139=VERTEX_POINT ( 'NONE', #5263 ) ;
#8141=EDGE_CURVE ( 'NONE', #6378, #4688, #5230, .T. ) ;
#8156=EDGE_CURVE ( 'NONE', #7658, #6819, #4904, .T. ) ;
#8166=ORIENTED_EDGE ( 'NONE', *, *, #2744, .T. ) ;
#8174=VECTOR ( 'NONE', #6220, 1000.000000000000114 ) ;
#8198=AXIS2_PLACEMENT_3D ( 'NONE', #6105, #408, #1833 ) ;
ENDSEC;
END-ISO-10303-21;
